ISO-10303-21;
HEADER;
FILE_DESCRIPTION (('STEP AP214'),
    '1' );
FILE_NAME ('circlip for shafts normal_din_Circlip DIN 471 - 22 x 1.2.step',
    '2026-10-08T11:45:07',
    ( '' ),
    ( '' ),
    'SwSTEP 2.0',
    'SolidWorks 2026',
    '' );
FILE_SCHEMA (( 'AUTOMOTIVE_DESIGN' ));
ENDSEC;

DATA;
#4=CYLINDRICAL_SURFACE ( 'NONE', #27715, 12.55910585664918422 ) ;
#166=DIRECTION ( 'NONE',  ( 1.000000000000000000, 0.000000000000000000, 0.000000000000000000 ) ) ;
#377=FACE_OUTER_BOUND ( 'NONE', #25940, .T. ) ;
#391=CARTESIAN_POINT ( 'NONE',  ( 0.000000000000000000, 0.7408941433508176022, -1.199999999999999956 ) ) ;
#469=CARTESIAN_POINT ( 'NONE',  ( 4.121423858225410797, -12.61643262889541006, -1.199999999999999956 ) ) ;
#604=DIRECTION ( 'NONE',  ( -0.000000000000000000, -0.000000000000000000, -1.000000000000000000 ) ) ;
#694=ORIENTED_EDGE ( 'NONE', *, *, #24852, .F. ) ;
#770=VECTOR ( 'NONE', #18859, 1000.000000000000000 ) ;
#813=CARTESIAN_POINT ( 'NONE',  ( 6.896599878636567205, -12.98179148322719101, -1.199999999999999956 ) ) ;
#843=ADVANCED_FACE ( 'NONE', ( #377 ), #20735, .F. ) ;
#898=DIRECTION ( 'NONE',  ( 1.000000000000000000, 0.000000000000000000, 0.000000000000000000 ) ) ;
#977=CIRCLE ( 'NONE', #4471, 10.50000000000000178 ) ;
#1031=DIRECTION ( 'NONE',  ( 1.000000000000000000, 0.000000000000000000, 0.000000000000000000 ) ) ;
#1100=CARTESIAN_POINT ( 'NONE',  ( -5.639656061357299244, -10.48075544252182922, -1.199999999999999956 ) ) ;
#1251=EDGE_CURVE ( 'NONE', #4089, #31991, #23727, .T. ) ;
#1321=CIRCLE ( 'NONE', #6892, 1.000000000000000444 ) ;
#1352=AXIS2_PLACEMENT_3D ( 'NONE', #10473, #36866, #36639 ) ;
#1442=DIRECTION ( 'NONE',  ( 0.1305261922200494362, 0.9914448613738107152, 0.000000000000000000 ) ) ;
#1451=VERTEX_POINT ( 'NONE', #27857 ) ;
#1529=AXIS2_PLACEMENT_3D ( 'NONE', #17939, #37941, #11353 ) ;
#1551=CARTESIAN_POINT ( 'NONE',  ( -3.983177536951265640, -13.66651769228263191, -1.199999999999999956 ) ) ;
#1623=( GEOMETRIC_REPRESENTATION_CONTEXT ( 3 ) GLOBAL_UNCERTAINTY_ASSIGNED_CONTEXT ( ( #40903 ) ) GLOBAL_UNIT_ASSIGNED_CONTEXT ( ( #23045, #2897, #33672 ) ) REPRESENTATION_CONTEXT ( 'NONE', 'WORKASPACE' ) );
#1709=CARTESIAN_POINT ( 'NONE',  ( -3.983177536951265640, -13.66651769228263191, 0.000000000000000000 ) ) ;
#1794=AXIS2_PLACEMENT_3D ( 'NONE', #23744, #37015, #33964 ) ;
#1890=DIRECTION ( 'NONE',  ( 0.000000000000000000, 0.000000000000000000, 1.000000000000000000 ) ) ;
#1895=DIRECTION ( 'NONE',  ( 0.000000000000000000, 0.000000000000000000, 1.000000000000000000 ) ) ;
#1905=EDGE_LOOP ( 'NONE', ( #41869, #18159, #28124, #17802 ) ) ;
#1942=DIRECTION ( 'NONE',  ( 1.000000000000000000, 0.000000000000000000, 0.000000000000000000 ) ) ;
#2112=ORIENTED_EDGE ( 'NONE', *, *, #23938, .F. ) ;
#2135=EDGE_LOOP ( 'NONE', ( #36274, #8758, #39515, #37056, #6586, #37781, #26710, #12953, #23832, #37803, #32282, #16023, #34985, #3847, #8009, #29186 ) ) ;
#2279=ADVANCED_FACE ( 'NONE', ( #13805 ), #27101, .F. ) ;
#2427=VERTEX_POINT ( 'NONE', #8674 ) ;
#2436=CARTESIAN_POINT ( 'NONE',  ( 0.000000000000000000, 0.7408941433508176022, -1.199999999999999956 ) ) ;
#2530=VERTEX_POINT ( 'NONE', #9543 ) ;
#2579=FACE_OUTER_BOUND ( 'NONE', #11382, .T. ) ;
#2599=ORIENTED_EDGE ( 'NONE', *, *, #41735, .T. ) ;
#2645=ORIENTED_EDGE ( 'NONE', *, *, #16879, .F. ) ;
#2657=CARTESIAN_POINT ( 'NONE',  ( 2.600000000000000533, -12.75000000000000000, -1.199999999999999956 ) ) ;
#2701=ORIENTED_EDGE ( 'NONE', *, *, #26748, .F. ) ;
#2790=DIRECTION ( 'NONE',  ( 0.000000000000000000, 0.000000000000000000, 1.000000000000000000 ) ) ;
#2798=CARTESIAN_POINT ( 'NONE',  ( 0.000000000000000000, 0.7408941433508176022, 0.000000000000000000 ) ) ;
#2838=LINE ( 'NONE', #29941, #29689 ) ;
#2843=ADVANCED_FACE ( 'NONE', ( #18927, #32184, #37854 ), #28929, .F. ) ;
#2887=ORIENTED_EDGE ( 'NONE', *, *, #22540, .F. ) ;
#2891=EDGE_CURVE ( 'NONE', #21142, #13428, #13691, .T. ) ;
#2897=( NAMED_UNIT ( * ) PLANE_ANGLE_UNIT ( ) SI_UNIT ( $, .RADIAN. ) );
#2956=AXIS2_PLACEMENT_3D ( 'NONE', #10609, #37211, #30256 ) ;
#2959=DIRECTION ( 'NONE',  ( 0.000000000000000000, 0.000000000000000000, 1.000000000000000000 ) ) ;
#2973=VERTEX_POINT ( 'NONE', #29149 ) ;
#3002=FACE_OUTER_BOUND ( 'NONE', #7141, .T. ) ;
#3045=CARTESIAN_POINT ( 'NONE',  ( -0.5999999999999996447, -12.75000000000000000, -1.199999999999999956 ) ) ;
#3137=CIRCLE ( 'NONE', #41502, 12.55910585664918422 ) ;
#3175=VECTOR ( 'NONE', #16415, 1000.000000000000000 ) ;
#3211=VERTEX_POINT ( 'NONE', #34325 ) ;
#3292=AXIS2_PLACEMENT_3D ( 'NONE', #38380, #35105, #1942 ) ;
#3318=ORIENTED_EDGE ( 'NONE', *, *, #18428, .T. ) ;
#3363=EDGE_LOOP ( 'NONE', ( #11749, #25000 ) ) ;
#3372=FACE_OUTER_BOUND ( 'NONE', #28907, .T. ) ;
#3433=CARTESIAN_POINT ( 'NONE',  ( 3.983177536951266529, -13.66651769228263191, -1.199999999999999956 ) ) ;
#3489=CIRCLE ( 'NONE', #18214, 0.7500000000000006661 ) ;
#3564=LINE ( 'NONE', #26726, #40049 ) ;
#3666=CARTESIAN_POINT ( 'NONE',  ( 0.2142857142857142738, -10.49781318335647917, -1.199999999999999956 ) ) ;
#3685=EDGE_LOOP ( 'NONE', ( #20062, #30869, #13628, #17022 ) ) ;
#3770=CARTESIAN_POINT ( 'NONE',  ( 0.2142857142857142738, -10.49781318335647917, 0.000000000000000000 ) ) ;
#3791=AXIS2_PLACEMENT_3D ( 'NONE', #7208, #20567, #17905 ) ;
#3798=VERTEX_POINT ( 'NONE', #37972 ) ;
#3840=LINE ( 'NONE', #6922, #23106 ) ;
#3847=ORIENTED_EDGE ( 'NONE', *, *, #36443, .T. ) ;
#3851=EDGE_CURVE ( 'NONE', #16399, #3211, #24715, .T. ) ;
#3852=CARTESIAN_POINT ( 'NONE',  ( 0.000000000000000000, 0.000000000000000000, 0.000000000000000000 ) ) ;
#3901=DIRECTION ( 'NONE',  ( 1.000000000000000000, 0.000000000000000000, 0.000000000000000000 ) ) ;
#4033=DIRECTION ( 'NONE',  ( 1.000000000000000000, 0.000000000000000000, 0.000000000000000000 ) ) ;
#4057=EDGE_CURVE ( 'NONE', #26713, #31572, #12963, .T. ) ;
#4089=VERTEX_POINT ( 'NONE', #31808 ) ;
#4134=EDGE_CURVE ( 'NONE', #1451, #35327, #15028, .T. ) ;
#4147=CARTESIAN_POINT ( 'NONE',  ( 0.000000000000000000, 0.000000000000000000, -1.199999999999999956 ) ) ;
#4148=EDGE_LOOP ( 'NONE', ( #30828, #26318, #32191, #694 ) ) ;
#4249=UNCERTAINTY_MEASURE_WITH_UNIT (LENGTH_MEASURE( 1.000000000000000082E-05 ), #41344, 'distance_accuracy_value', 'NONE');
#4325=EDGE_CURVE ( 'NONE', #2530, #30690, #31805, .T. ) ;
#4329=EDGE_CURVE ( 'NONE', #16399, #33425, #26222, .T. ) ;
#4456=CARTESIAN_POINT ( 'NONE',  ( -3.983177536951265640, -13.66651769228263191, -1.199999999999999956 ) ) ;
#4471=AXIS2_PLACEMENT_3D ( 'NONE', #38743, #38955, #42440 ) ;
#4489=AXIS2_PLACEMENT_3D ( 'NONE', #19385, #33299, #6666 ) ;
#4570=CIRCLE ( 'NONE', #29692, 1.000000000000000666 ) ;
#4624=VECTOR ( 'NONE', #16100, 1000.000000000000000 ) ;
#4633=LINE ( 'NONE', #17180, #37977 ) ;
#4653=FACE_OUTER_BOUND ( 'NONE', #17606, .T. ) ;
#4739=CARTESIAN_POINT ( 'NONE',  ( -0.2142857142857142738, -10.49781318335647917, 0.000000000000000000 ) ) ;
#4811=ORIENTED_EDGE ( 'NONE', *, *, #19772, .F. ) ;
#4845=AXIS2_PLACEMENT_3D ( 'NONE', #22644, #12800, #32643 ) ;
#4910=VECTOR ( 'NONE', #21425, 1000.000000000000000 ) ;
#4923=DIRECTION ( 'NONE',  ( 1.000000000000000000, 0.000000000000000000, 0.000000000000000000 ) ) ;
#4924=CARTESIAN_POINT ( 'NONE',  ( 0.000000000000000000, 0.7408941433508176022, 0.000000000000000000 ) ) ;
#4951=ORIENTED_EDGE ( 'NONE', *, *, #36443, .F. ) ;
#5012=CARTESIAN_POINT ( 'NONE',  ( 3.983177536951266529, -13.66651769228263191, 0.000000000000000000 ) ) ;
#5020=DIRECTION ( 'NONE',  ( 1.000000000000000000, 0.000000000000000000, 0.000000000000000000 ) ) ;
#5035=CIRCLE ( 'NONE', #22487, 12.55910585664918422 ) ;
#5063=CARTESIAN_POINT ( 'NONE',  ( 5.639656061357294803, -10.48075544252183100, -1.199999999999999956 ) ) ;
#5099=ORIENTED_EDGE ( 'NONE', *, *, #11532, .T. ) ;
#5219=CARTESIAN_POINT ( 'NONE',  ( -3.239593890920906993, -13.56862304811759223, 0.000000000000000000 ) ) ;
#5252=CIRCLE ( 'NONE', #28972, 10.50000000000000178 ) ;
#5310=ORIENTED_EDGE ( 'NONE', *, *, #24792, .F. ) ;
#5334=EDGE_LOOP ( 'NONE', ( #7355, #22700 ) ) ;
#5445=FACE_OUTER_BOUND ( 'NONE', #7909, .T. ) ;
#5665=CARTESIAN_POINT ( 'NONE',  ( 0.3000000000000028200, -14.69693845669907084, -1.199999999999999956 ) ) ;
#5828=EDGE_CURVE ( 'NONE', #16799, #12487, #35370, .T. ) ;
#5835=FACE_OUTER_BOUND ( 'NONE', #3685, .T. ) ;
#5899=VERTEX_POINT ( 'NONE', #17962 ) ;
#5975=CIRCLE ( 'NONE', #35925, 10.50000000000000178 ) ;
#6081=EDGE_CURVE ( 'NONE', #41098, #39261, #22374, .T. ) ;
#6116=AXIS2_PLACEMENT_3D ( 'NONE', #40128, #27290, #13994 ) ;
#6167=DIRECTION ( 'NONE',  ( 0.000000000000000000, 0.000000000000000000, 1.000000000000000000 ) ) ;
#6183=EDGE_CURVE ( 'NONE', #30690, #36459, #3489, .T. ) ;
#6196=EDGE_CURVE ( 'NONE', #14824, #27141, #9092, .T. ) ;
#6203=LINE ( 'NONE', #31982, #33687 ) ;
#6222=CARTESIAN_POINT ( 'NONE',  ( -3.413765605486552168, -14.29811891091961407, -1.199999999999999956 ) ) ;
#6264=ADVANCED_FACE ( 'NONE', ( #3002 ), #30108, .T. ) ;
#6336=CYLINDRICAL_SURFACE ( 'NONE', #13874, 10.50000000000000178 ) ;
#6373=CYLINDRICAL_SURFACE ( 'NONE', #8190, 0.7500000000000006661 ) ;
#6513=DIRECTION ( 'NONE',  ( 1.000000000000000000, 0.000000000000000000, 0.000000000000000000 ) ) ;
#6524=CARTESIAN_POINT ( 'NONE',  ( 4.121423858225410797, -12.61643262889541006, 0.000000000000000000 ) ) ;
#6586=ORIENTED_EDGE ( 'NONE', *, *, #4325, .T. ) ;
#6666=DIRECTION ( 'NONE',  ( 1.000000000000000000, 0.000000000000000000, 0.000000000000000000 ) ) ;
#6674=VECTOR ( 'NONE', #30099, 1000.000000000000114 ) ;
#6691=VECTOR ( 'NONE', #11754, 1000.000000000000000 ) ;
#6786=ADVANCED_FACE ( 'NONE', ( #4653 ), #34769, .T. ) ;
#6822=CARTESIAN_POINT ( 'NONE',  ( 5.639656061357294803, -10.48075544252183100, 0.000000000000000000 ) ) ;
#6892=AXIS2_PLACEMENT_3D ( 'NONE', #8756, #41907, #32307 ) ;
#6922=CARTESIAN_POINT ( 'NONE',  ( 4.121423858225410797, -12.61643262889541006, 0.000000000000000000 ) ) ;
#7141=EDGE_LOOP ( 'NONE', ( #37664, #38819, #32957, #42464 ) ) ;
#7142=LINE ( 'NONE', #40510, #17170 ) ;
#7170=ADVANCED_FACE ( 'NONE', ( #16429 ), #4, .T. ) ;
#7185=ORIENTED_EDGE ( 'NONE', *, *, #11532, .F. ) ;
#7191=COLOUR_RGB ( '', 0.08235294, 0.09019608, 0.10196078) ;
#7206=AXIS2_PLACEMENT_3D ( 'NONE', #27818, #18031, #40861 ) ;
#7208=CARTESIAN_POINT ( 'NONE',  ( 0.000000000000000000, 0.000000000000000000, -1.199999999999999956 ) ) ;
#7240=AXIS2_PLACEMENT_3D ( 'NONE', #2798, #23360, #22513 ) ;
#7279=ORIENTED_EDGE ( 'NONE', *, *, #33479, .F. ) ;
#7355=ORIENTED_EDGE ( 'NONE', *, *, #28512, .T. ) ;
#7403=CIRCLE ( 'NONE', #11608, 1.000000000000000666 ) ;
#7584=AXIS2_PLACEMENT_3D ( 'NONE', #5219, #41656, #12801 ) ;
#7680=EDGE_CURVE ( 'NONE', #31449, #36459, #31619, .T. ) ;
#7727=ORIENTED_EDGE ( 'NONE', *, *, #19339, .F. ) ;
#7895=ORIENTED_EDGE ( 'NONE', *, *, #33455, .F. ) ;
#7897=PLANE ( 'NONE',  #40268 ) ;
#7909=EDGE_LOOP ( 'NONE', ( #26389, #30001, #8771, #2701 ) ) ;
#7949=ORIENTED_EDGE ( 'NONE', *, *, #23633, .F. ) ;
#7978=DIRECTION ( 'NONE',  ( 0.000000000000000000, 0.000000000000000000, 1.000000000000000000 ) ) ;
#8009=ORIENTED_EDGE ( 'NONE', *, *, #6081, .T. ) ;
#8064=DIRECTION ( 'NONE',  ( 0.000000000000000000, 0.000000000000000000, 1.000000000000000000 ) ) ;
#8076=EDGE_CURVE ( 'NONE', #36459, #18380, #3840, .T. ) ;
#8119=DIRECTION ( 'NONE',  ( 1.000000000000000000, 0.000000000000000000, 0.000000000000000000 ) ) ;
#8176=CARTESIAN_POINT ( 'NONE',  ( -0.2142857142857142738, -10.49781318335647917, 0.000000000000000000 ) ) ;
#8190=AXIS2_PLACEMENT_3D ( 'NONE', #13383, #19722, #29518 ) ;
#8207=DIRECTION ( 'NONE',  ( 0.000000000000000000, 0.000000000000000000, 1.000000000000000000 ) ) ;
#8214=EDGE_CURVE ( 'NONE', #39261, #35327, #27674, .T. ) ;
#8339=VECTOR ( 'NONE', #15547, 1000.000000000000000 ) ;
#8417=FILL_AREA_STYLE ('',( #15230 ) ) ;
#8524=DIRECTION ( 'NONE',  ( 0.000000000000000000, 0.000000000000000000, 1.000000000000000000 ) ) ;
#8672=VECTOR ( 'NONE', #8524, 1000.000000000000000 ) ;
#8674=CARTESIAN_POINT ( 'NONE',  ( 0.3000000000000028200, -14.69693845669907084, -1.199999999999999956 ) ) ;
#8692=DIRECTION ( 'NONE',  ( 1.000000000000000000, 0.000000000000000000, 0.000000000000000000 ) ) ;
#8756=CARTESIAN_POINT ( 'NONE',  ( -1.600000000000000089, -12.75000000000000000, 0.000000000000000000 ) ) ;
#8757=DIRECTION ( 'NONE',  ( 1.000000000000000000, 0.000000000000000000, 0.000000000000000000 ) ) ;
#8758=ORIENTED_EDGE ( 'NONE', *, *, #22540, .T. ) ;
#8767=LINE ( 'NONE', #22336, #18257 ) ;
#8771=ORIENTED_EDGE ( 'NONE', *, *, #3851, .T. ) ;
#8838=CIRCLE ( 'NONE', #24932, 12.55910585664918422 ) ;
#8865=PLANE ( 'NONE',  #10210 ) ;
#8912=CYLINDRICAL_SURFACE ( 'NONE', #17853, 1.000000000000000666 ) ;
#9092=CIRCLE ( 'NONE', #29322, 12.55910585664918422 ) ;
#9093=ADVANCED_FACE ( 'NONE', ( #34682 ), #28155, .F. ) ;
#9145=DIRECTION ( 'NONE',  ( 0.000000000000000000, 0.000000000000000000, 1.000000000000000000 ) ) ;
#9205=CARTESIAN_POINT ( 'NONE',  ( 0.000000000000000000, 0.7408941433508176022, -1.199999999999999956 ) ) ;
#9260=ORIENTED_EDGE ( 'NONE', *, *, #41455, .F. ) ;
#9410=CIRCLE ( 'NONE', #10129, 2.799122904894268959 ) ;
#9462=AXIS2_PLACEMENT_3D ( 'NONE', #4924, #8207, #34817 ) ;
#9543=CARTESIAN_POINT ( 'NONE',  ( 0.3000000000000028200, -14.69693845669907084, 0.000000000000000000 ) ) ;
#9608=LINE ( 'NONE', #3666, #35365 ) ;
#9641=DIRECTION ( 'NONE',  ( 1.000000000000000000, 0.000000000000000000, 0.000000000000000000 ) ) ;
#9773=ORIENTED_EDGE ( 'NONE', *, *, #4057, .T. ) ;
#10007=EDGE_CURVE ( 'NONE', #21541, #28496, #14314, .T. ) ;
#10095=DIRECTION ( 'NONE',  ( 0.02040816326530612776, -0.9997917317482359900, 0.000000000000000000 ) ) ;
#10106=DIRECTION ( 'NONE',  ( 0.02040816326530612776, 0.9997917317482359900, -0.000000000000000000 ) ) ;
#10129=AXIS2_PLACEMENT_3D ( 'NONE', #14552, #40904, #27859 ) ;
#10189=ORIENTED_EDGE ( 'NONE', *, *, #1251, .F. ) ;
#10210=AXIS2_PLACEMENT_3D ( 'NONE', #41142, #21587, #1442 ) ;
#10212=AXIS2_PLACEMENT_3D ( 'NONE', #35737, #9145, #28604 ) ;
#10213=DIRECTION ( 'NONE',  ( 1.000000000000000000, 0.000000000000000000, 0.000000000000000000 ) ) ;
#10233=DIRECTION ( 'NONE',  ( 0.000000000000000000, 0.000000000000000000, 1.000000000000000000 ) ) ;
#10393=PRODUCT_DEFINITION_CONTEXT ( 'detailed design', #22886, 'design' ) ;
#10395=EDGE_LOOP ( 'NONE', ( #7185, #40809, #2645, #31258, #12083, #28003, #9260, #27534, #20029, #33412, #39773, #30040, #21251, #19062, #16185, #7279 ) ) ;
#10473=CARTESIAN_POINT ( 'NONE',  ( 6.896599878636567205, -12.98179148322719101, 0.000000000000000000 ) ) ;
#10568=EDGE_CURVE ( 'NONE', #38781, #38690, #42122, .T. ) ;
#10609=CARTESIAN_POINT ( 'NONE',  ( 0.000000000000000000, 0.000000000000000000, -1.199999999999999956 ) ) ;
#10678=EDGE_CURVE ( 'NONE', #12487, #12248, #8767, .T. ) ;
#10777=FILL_AREA_STYLE ('',( #28025 ) ) ;
#11069=AXIS2_PLACEMENT_3D ( 'NONE', #20377, #40393, #13389 ) ;
#11086=CARTESIAN_POINT ( 'NONE',  ( 0.2142857142857142738, -10.49781318335647917, -1.199999999999999956 ) ) ;
#11136=VERTEX_POINT ( 'NONE', #32654 ) ;
#11145=CARTESIAN_POINT ( 'NONE',  ( 0.000000000000000000, 0.000000000000000000, -1.199999999999999956 ) ) ;
#11308=DIRECTION ( 'NONE',  ( 1.000000000000000000, 0.000000000000000000, 0.000000000000000000 ) ) ;
#11353=DIRECTION ( 'NONE',  ( 1.000000000000000000, 0.000000000000000000, 0.000000000000000000 ) ) ;
#11382=EDGE_LOOP ( 'NONE', ( #31143, #30136, #31823, #33171 ) ) ;
#11391=CIRCLE ( 'NONE', #26021, 1.000000000000000666 ) ;
#11394=EDGE_CURVE ( 'NONE', #3798, #2973, #26041, .T. ) ;
#11464=CARTESIAN_POINT ( 'NONE',  ( 3.413765605486547727, -14.29811891091961229, 0.000000000000000000 ) ) ;
#11532=EDGE_CURVE ( 'NONE', #1451, #4089, #14116, .T. ) ;
#11608=AXIS2_PLACEMENT_3D ( 'NONE', #18997, #25319, #8692 ) ;
#11749=ORIENTED_EDGE ( 'NONE', *, *, #30910, .F. ) ;
#11754=DIRECTION ( 'NONE',  ( 0.000000000000000000, 0.000000000000000000, 1.000000000000000000 ) ) ;
#11758=CARTESIAN_POINT ( 'NONE',  ( -0.2142857142857142738, -10.49781318335647917, -1.199999999999999956 ) ) ;
#11857=DIRECTION ( 'NONE',  ( 0.000000000000000000, 0.000000000000000000, 1.000000000000000000 ) ) ;
#11892=CARTESIAN_POINT ( 'NONE',  ( 1.600000000000000089, -12.75000000000000000, -1.199999999999999956 ) ) ;
#11908=ORIENTED_EDGE ( 'NONE', *, *, #8214, .F. ) ;
#11936=SURFACE_SIDE_STYLE ('',( #28083 ) ) ;
#11961=DIRECTION ( 'NONE',  ( 1.000000000000000000, 0.000000000000000000, 0.000000000000000000 ) ) ;
#12083=ORIENTED_EDGE ( 'NONE', *, *, #32837, .F. ) ;
#12103=DIRECTION ( 'NONE',  ( 1.000000000000000000, 0.000000000000000000, 0.000000000000000000 ) ) ;
#12248=VERTEX_POINT ( 'NONE', #3770 ) ;
#12281=AXIS2_PLACEMENT_3D ( 'NONE', #35541, #12454, #5020 ) ;
#12410=AXIS2_PLACEMENT_3D ( 'NONE', #25428, #25850, #41962 ) ;
#12454=DIRECTION ( 'NONE',  ( -0.000000000000000000, -0.000000000000000000, -1.000000000000000000 ) ) ;
#12475=CARTESIAN_POINT ( 'NONE',  ( 3.239593890920906993, -13.56862304811759223, -1.199999999999999956 ) ) ;
#12487=VERTEX_POINT ( 'NONE', #14521 ) ;
#12620=CARTESIAN_POINT ( 'NONE',  ( 12.55910585664918422, 0.7408941433508176022, -1.199999999999999956 ) ) ;
#12647=VECTOR ( 'NONE', #18101, 1000.000000000000114 ) ;
#12744=FACE_BOUND ( 'NONE', #3363, .T. ) ;
#12800=DIRECTION ( 'NONE',  ( 0.000000000000000000, 0.000000000000000000, 1.000000000000000000 ) ) ;
#12801=DIRECTION ( 'NONE',  ( 1.000000000000000000, 0.000000000000000000, 0.000000000000000000 ) ) ;
#12842=CIRCLE ( 'NONE', #7240, 12.55910585664918422 ) ;
#12906=COLOUR_RGB ( '', 0.08235294, 0.09019608, 0.10196078) ;
#12953=ORIENTED_EDGE ( 'NONE', *, *, #19772, .T. ) ;
#12963=CIRCLE ( 'NONE', #17153, 1.000000000000000444 ) ;
#13063=DIRECTION ( 'NONE',  ( 1.000000000000000000, 0.000000000000000000, 0.000000000000000000 ) ) ;
#13177=VERTEX_POINT ( 'NONE', #36155 ) ;
#13304=VECTOR ( 'NONE', #20448, 1000.000000000000000 ) ;
#13383=CARTESIAN_POINT ( 'NONE',  ( -3.239593890920906993, -13.56862304811759223, -1.199999999999999956 ) ) ;
#13389=DIRECTION ( 'NONE',  ( 1.000000000000000000, 0.000000000000000000, 0.000000000000000000 ) ) ;
#13428=VERTEX_POINT ( 'NONE', #31358 ) ;
#13494=DIRECTION ( 'NONE',  ( 1.000000000000000000, 0.000000000000000000, 0.000000000000000000 ) ) ;
#13515=ORIENTED_EDGE ( 'NONE', *, *, #16879, .T. ) ;
#13552=AXIS2_PLACEMENT_3D ( 'NONE', #3852, #14597, #10213 ) ;
#13599=FACE_OUTER_BOUND ( 'NONE', #28797, .T. ) ;
#13628=ORIENTED_EDGE ( 'NONE', *, *, #23425, .T. ) ;
#13670=ORIENTED_EDGE ( 'NONE', *, *, #4134, .T. ) ;
#13691=CIRCLE ( 'NONE', #9462, 12.55910585664918422 ) ;
#13805=FACE_OUTER_BOUND ( 'NONE', #31384, .T. ) ;
#13874=AXIS2_PLACEMENT_3D ( 'NONE', #11145, #8064, #3901 ) ;
#13904=UNCERTAINTY_MEASURE_WITH_UNIT (LENGTH_MEASURE( 1.000000000000000082E-05 ), #34536, 'distance_accuracy_value', 'NONE');
#13994=DIRECTION ( 'NONE',  ( 1.000000000000000000, 0.000000000000000000, 0.000000000000000000 ) ) ;
#14036=CARTESIAN_POINT ( 'NONE',  ( 0.000000000000000000, 0.000000000000000000, -1.199999999999999956 ) ) ;
#14110=CARTESIAN_POINT ( 'NONE',  ( -0.2999999999999999889, -14.69693845669906906, -1.199999999999999956 ) ) ;
#14116=CIRCLE ( 'NONE', #40536, 10.50000000000000178 ) ;
#14130=ORIENTED_EDGE ( 'NONE', *, *, #10568, .F. ) ;
#14215=CIRCLE ( 'NONE', #39236, 1.000000000000000666 ) ;
#14314=LINE ( 'NONE', #4456, #18910 ) ;
#14365=FACE_OUTER_BOUND ( 'NONE', #29197, .T. ) ;
#14445=DIRECTION ( 'NONE',  ( -0.000000000000000000, -0.000000000000000000, -1.000000000000000000 ) ) ;
#14479=CARTESIAN_POINT ( 'NONE',  ( 0.000000000000000000, 0.000000000000000000, -1.199999999999999956 ) ) ;
#14521=CARTESIAN_POINT ( 'NONE',  ( 0.2142857142857142738, -10.49781318335647917, -1.199999999999999956 ) ) ;
#14552=CARTESIAN_POINT ( 'NONE',  ( 6.896599878636567205, -12.98179148322719101, -1.199999999999999956 ) ) ;
#14597=DIRECTION ( 'NONE',  ( 0.000000000000000000, 0.000000000000000000, 1.000000000000000000 ) ) ;
#14598=CARTESIAN_POINT ( 'NONE',  ( -1.600000000000000089, -12.75000000000000000, -1.199999999999999956 ) ) ;
#14723=( NAMED_UNIT ( * ) SI_UNIT ( $, .STERADIAN. ) SOLID_ANGLE_UNIT ( ) );
#14733=DIRECTION ( 'NONE',  ( 0.000000000000000000, 0.000000000000000000, 1.000000000000000000 ) ) ;
#14768=ORIENTED_EDGE ( 'NONE', *, *, #32837, .T. ) ;
#14775=CARTESIAN_POINT ( 'NONE',  ( 1.600000000000000089, -12.75000000000000000, -1.199999999999999956 ) ) ;
#14824=VERTEX_POINT ( 'NONE', #15445 ) ;
#14915=ORIENTED_EDGE ( 'NONE', *, *, #36976, .F. ) ;
#15028=LINE ( 'NONE', #11758, #24829 ) ;
#15120=DIRECTION ( 'NONE',  ( -1.000000000000000000, 0.000000000000000000, 0.000000000000000000 ) ) ;
#15184=VERTEX_POINT ( 'NONE', #18693 ) ;
#15221=ORIENTED_EDGE ( 'NONE', *, *, #28143, .T. ) ;
#15230=FILL_AREA_STYLE_COLOUR ( '', #12906 ) ;
#15260=ADVANCED_FACE ( 'NONE', ( #41958 ), #25220, .F. ) ;
#15445=CARTESIAN_POINT ( 'NONE',  ( 5.639656061357294803, -10.48075544252183100, -1.199999999999999956 ) ) ;
#15527=CARTESIAN_POINT ( 'NONE',  ( 0.000000000000000000, 0.000000000000000000, 0.000000000000000000 ) ) ;
#15547=DIRECTION ( 'NONE',  ( 0.000000000000000000, 0.000000000000000000, 1.000000000000000000 ) ) ;
#15685=AXIS2_PLACEMENT_3D ( 'NONE', #813, #20511, #23780 ) ;
#15870=CIRCLE ( 'NONE', #40210, 0.7500000000000006661 ) ;
#15897=ORIENTED_EDGE ( 'NONE', *, *, #33479, .T. ) ;
#16023=ORIENTED_EDGE ( 'NONE', *, *, #32823, .T. ) ;
#16100=DIRECTION ( 'NONE',  ( 0.000000000000000000, 0.000000000000000000, 1.000000000000000000 ) ) ;
#16185=ORIENTED_EDGE ( 'NONE', *, *, #5828, .F. ) ;
#16197=EDGE_CURVE ( 'NONE', #13177, #12248, #38175, .T. ) ;
#16279=ADVANCED_FACE ( 'NONE', ( #5445 ), #41428, .T. ) ;
#16399=VERTEX_POINT ( 'NONE', #17426 ) ;
#16415=DIRECTION ( 'NONE',  ( 0.000000000000000000, 0.000000000000000000, 1.000000000000000000 ) ) ;
#16429=FACE_OUTER_BOUND ( 'NONE', #33776, .T. ) ;
#16488=LINE ( 'NONE', #41453, #8672 ) ;
#16531=FACE_OUTER_BOUND ( 'NONE', #39297, .T. ) ;
#16719=CIRCLE ( 'NONE', #1352, 2.799122904894268959 ) ;
#16785=CARTESIAN_POINT ( 'NONE',  ( -3.239593890920906993, -13.56862304811759223, -1.199999999999999956 ) ) ;
#16799=VERTEX_POINT ( 'NONE', #35870 ) ;
#16840=SHAPE_REPRESENTATION ( 'circlip for shafts normal_din_Circlip DIN 471 - 22 x 1.2', ( #13552 ), #1623 ) ;
#16879=EDGE_CURVE ( 'NONE', #24620, #27149, #40107, .T. ) ;
#17018=CARTESIAN_POINT ( 'NONE',  ( -4.121423858225412573, -12.61643262889541184, -1.199999999999999956 ) ) ;
#17022=ORIENTED_EDGE ( 'NONE', *, *, #11394, .F. ) ;
#17086=DIRECTION ( 'NONE',  ( 0.000000000000000000, 0.000000000000000000, 1.000000000000000000 ) ) ;
#17153=AXIS2_PLACEMENT_3D ( 'NONE', #14598, #1895, #11308 ) ;
#17170=VECTOR ( 'NONE', #23766, 1000.000000000000114 ) ;
#17180=CARTESIAN_POINT ( 'NONE',  ( -4.121423858225412573, -12.61643262889541184, 0.000000000000000000 ) ) ;
#17239=ORIENTED_EDGE ( 'NONE', *, *, #7680, .T. ) ;
#17292=AXIS2_PLACEMENT_3D ( 'NONE', #4147, #14445, #18179 ) ;
#17426=CARTESIAN_POINT ( 'NONE',  ( -5.639656061357299244, -10.48075544252182922, -1.199999999999999956 ) ) ;
#17519=EDGE_CURVE ( 'NONE', #23300, #21142, #8838, .T. ) ;
#17606=EDGE_LOOP ( 'NONE', ( #35259, #25658, #14768, #39154 ) ) ;
#17802=ORIENTED_EDGE ( 'NONE', *, *, #29587, .T. ) ;
#17853=AXIS2_PLACEMENT_3D ( 'NONE', #22263, #2959, #13063 ) ;
#17872=DIRECTION ( 'NONE',  ( 0.02040816326530612776, -0.9997917317482359900, 0.000000000000000000 ) ) ;
#17880=CARTESIAN_POINT ( 'NONE',  ( -3.413765605486552168, -14.29811891091961407, -1.199999999999999956 ) ) ;
#17905=DIRECTION ( 'NONE',  ( 1.000000000000000000, 0.000000000000000000, 0.000000000000000000 ) ) ;
#17910=ADVANCED_FACE ( 'NONE', ( #13599 ), #6373, .T. ) ;
#17939=CARTESIAN_POINT ( 'NONE',  ( -1.600000000000000089, -12.75000000000000000, -1.199999999999999956 ) ) ;
#17962=CARTESIAN_POINT ( 'NONE',  ( -2.600000000000000533, -12.75000000000000000, 0.000000000000000000 ) ) ;
#18000=VERTEX_POINT ( 'NONE', #19944 ) ;
#18031=DIRECTION ( 'NONE',  ( -0.9914448613738104932, -0.1305261922200512681, 0.000000000000000000 ) ) ;
#18101=DIRECTION ( 'NONE',  ( 0.02040816326530612776, 0.9997917317482359900, -0.000000000000000000 ) ) ;
#18159=ORIENTED_EDGE ( 'NONE', *, *, #7680, .F. ) ;
#18179=DIRECTION ( 'NONE',  ( 1.000000000000000000, 0.000000000000000000, 0.000000000000000000 ) ) ;
#18214=AXIS2_PLACEMENT_3D ( 'NONE', #43167, #10233, #20311 ) ;
#18257=VECTOR ( 'NONE', #35386, 1000.000000000000000 ) ;
#18295=EDGE_CURVE ( 'NONE', #18000, #31449, #15870, .T. ) ;
#18346=ORIENTED_EDGE ( 'NONE', *, *, #28512, .F. ) ;
#18352=ORIENTED_EDGE ( 'NONE', *, *, #19339, .T. ) ;
#18380=VERTEX_POINT ( 'NONE', #6524 ) ;
#18381=MECHANICAL_DESIGN_GEOMETRIC_PRESENTATION_REPRESENTATION('',(#30978),#26063);
#18428=EDGE_CURVE ( 'NONE', #12487, #2427, #9608, .T. ) ;
#18693=CARTESIAN_POINT ( 'NONE',  ( -12.55910585664918422, 0.7408941433508191565, -1.199999999999999956 ) ) ;
#18853=ORIENTED_EDGE ( 'NONE', *, *, #19708, .T. ) ;
#18859=DIRECTION ( 'NONE',  ( 0.000000000000000000, 0.000000000000000000, 1.000000000000000000 ) ) ;
#18910=VECTOR ( 'NONE', #31751, 1000.000000000000000 ) ;
#18926=DIRECTION ( 'NONE',  ( 0.000000000000000000, 0.000000000000000000, 1.000000000000000000 ) ) ;
#18927=FACE_BOUND ( 'NONE', #37026, .T. ) ;
#18974=EDGE_CURVE ( 'NONE', #21541, #24620, #25693, .T. ) ;
#18997=CARTESIAN_POINT ( 'NONE',  ( 1.600000000000000089, -12.75000000000000000, -1.199999999999999956 ) ) ;
#19062=ORIENTED_EDGE ( 'NONE', *, *, #18428, .F. ) ;
#19269=CIRCLE ( 'NONE', #12281, 2.799122904894268071 ) ;
#19339=EDGE_CURVE ( 'NONE', #42086, #5899, #19460, .T. ) ;
#19366=CARTESIAN_POINT ( 'NONE',  ( -4.121423858225412573, -12.61643262889541184, 0.000000000000000000 ) ) ;
#19385=CARTESIAN_POINT ( 'NONE',  ( 3.239593890920906993, -13.56862304811759223, -1.199999999999999956 ) ) ;
#19392=CARTESIAN_POINT ( 'NONE',  ( 12.55910585664918422, 0.7408941433508176022, -1.199999999999999956 ) ) ;
#19460=CIRCLE ( 'NONE', #11069, 1.000000000000000444 ) ;
#19592=AXIS2_PLACEMENT_3D ( 'NONE', #33145, #42949, #166 ) ;
#19700=EDGE_CURVE ( 'NONE', #5899, #42086, #1321, .T. ) ;
#19708=EDGE_CURVE ( 'NONE', #15184, #13428, #28635, .T. ) ;
#19722=DIRECTION ( 'NONE',  ( 0.000000000000000000, 0.000000000000000000, 1.000000000000000000 ) ) ;
#19772=EDGE_CURVE ( 'NONE', #18380, #23300, #16719, .T. ) ;
#19869=LINE ( 'NONE', #5665, #34287 ) ;
#19944=CARTESIAN_POINT ( 'NONE',  ( 3.413765605486547727, -14.29811891091961229, -1.199999999999999956 ) ) ;
#20029=ORIENTED_EDGE ( 'NONE', *, *, #6196, .F. ) ;
#20062=ORIENTED_EDGE ( 'NONE', *, *, #26147, .F. ) ;
#20197=LINE ( 'NONE', #39976, #30772 ) ;
#20250=FACE_OUTER_BOUND ( 'NONE', #27654, .T. ) ;
#20311=DIRECTION ( 'NONE',  ( -1.000000000000000000, 0.000000000000000000, 0.000000000000000000 ) ) ;
#20377=CARTESIAN_POINT ( 'NONE',  ( -1.600000000000000089, -12.75000000000000000, 0.000000000000000000 ) ) ;
#20448=DIRECTION ( 'NONE',  ( 0.000000000000000000, 0.000000000000000000, 1.000000000000000000 ) ) ;
#20511=DIRECTION ( 'NONE',  ( 0.000000000000000000, 0.000000000000000000, 1.000000000000000000 ) ) ;
#20567=DIRECTION ( 'NONE',  ( 0.000000000000000000, 0.000000000000000000, 1.000000000000000000 ) ) ;
#20613=VECTOR ( 'NONE', #28619, 1000.000000000000000 ) ;
#20676=DIRECTION ( 'NONE',  ( 0.000000000000000000, 0.000000000000000000, 1.000000000000000000 ) ) ;
#20735=CYLINDRICAL_SURFACE ( 'NONE', #15685, 2.799122904894268959 ) ;
#20745=CARTESIAN_POINT ( 'NONE',  ( -0.5999999999999996447, -12.75000000000000000, 0.000000000000000000 ) ) ;
#20811=ADVANCED_FACE ( 'NONE', ( #3372 ), #30032, .F. ) ;
#20825=DIRECTION ( 'NONE',  ( -0.000000000000000000, -0.000000000000000000, -1.000000000000000000 ) ) ;
#20853=ADVANCED_BREP_SHAPE_REPRESENTATION ( '', ( #27502, #13552 ), #1623 ) ;
#20873=DIRECTION ( 'NONE',  ( 0.000000000000000000, 0.000000000000000000, 1.000000000000000000 ) ) ;
#21074=SURFACE_STYLE_FILL_AREA ( #10777 ) ;
#21122=ORIENTED_EDGE ( 'NONE', *, *, #16197, .F. ) ;
#21142=VERTEX_POINT ( 'NONE', #41244 ) ;
#21146=DIRECTION ( 'NONE',  ( -0.9997917317482359900, -0.02040816326530612776, 0.000000000000000000 ) ) ;
#21251=ORIENTED_EDGE ( 'NONE', *, *, #29979, .F. ) ;
#21304=ADVANCED_FACE ( 'NONE', ( #5835 ), #8912, .F. ) ;
#21341=DIRECTION ( 'NONE',  ( 1.000000000000000000, 0.000000000000000000, -0.000000000000000000 ) ) ;
#21425=DIRECTION ( 'NONE',  ( 0.000000000000000000, 0.000000000000000000, 1.000000000000000000 ) ) ;
#21521=CIRCLE ( 'NONE', #23582, 14.70000000000000107 ) ;
#21541=VERTEX_POINT ( 'NONE', #1551 ) ;
#21587=DIRECTION ( 'NONE',  ( 0.9914448613738107152, -0.1305261922200494362, 0.000000000000000000 ) ) ;
#21691=DIRECTION ( 'NONE',  ( 0.02040816326530612776, 0.9997917317482359900, 0.000000000000000000 ) ) ;
#21784=PRESENTATION_STYLE_ASSIGNMENT (( #31346 ) ) ;
#21970=( GEOMETRIC_REPRESENTATION_CONTEXT ( 3 ) GLOBAL_UNCERTAINTY_ASSIGNED_CONTEXT ( ( #4249 ) ) GLOBAL_UNIT_ASSIGNED_CONTEXT ( ( #41344, #37649, #24398 ) ) REPRESENTATION_CONTEXT ( 'NONE', 'WORKASPACE' ) );
#22015=ORIENTED_EDGE ( 'NONE', *, *, #4057, .F. ) ;
#22112=CARTESIAN_POINT ( 'NONE',  ( 0.000000000000000000, 0.000000000000000000, -1.199999999999999956 ) ) ;
#22263=CARTESIAN_POINT ( 'NONE',  ( 1.600000000000000089, -12.75000000000000000, -1.199999999999999956 ) ) ;
#22336=CARTESIAN_POINT ( 'NONE',  ( 0.2142857142857142738, -10.49781318335647917, -1.199999999999999956 ) ) ;
#22374=CIRCLE ( 'NONE', #36956, 14.70000000000000107 ) ;
#22487=AXIS2_PLACEMENT_3D ( 'NONE', #9205, #42356, #9641 ) ;
#22513=DIRECTION ( 'NONE',  ( 1.000000000000000000, 0.000000000000000000, 0.000000000000000000 ) ) ;
#22540=EDGE_CURVE ( 'NONE', #31991, #13177, #977, .T. ) ;
#22591=DIRECTION ( 'NONE',  ( 1.000000000000000000, 0.000000000000000000, 0.000000000000000000 ) ) ;
#22644=CARTESIAN_POINT ( 'NONE',  ( -1.600000000000000089, -12.75000000000000000, -1.199999999999999956 ) ) ;
#22700=ORIENTED_EDGE ( 'NONE', *, *, #26147, .T. ) ;
#22858=ORIENTED_EDGE ( 'NONE', *, *, #10678, .F. ) ;
#22886=APPLICATION_CONTEXT ( 'automotive_design' ) ;
#23005=EDGE_LOOP ( 'NONE', ( #36962, #24531, #33491, #21122 ) ) ;
#23045=( LENGTH_UNIT ( ) NAMED_UNIT ( * ) SI_UNIT ( .MILLI., .METRE. ) );
#23106=VECTOR ( 'NONE', #23330, 1000.000000000000114 ) ;
#23300=VERTEX_POINT ( 'NONE', #6822 ) ;
#23330=DIRECTION ( 'NONE',  ( 0.1305261922200494362, 0.9914448613738107152, -0.000000000000000000 ) ) ;
#23360=DIRECTION ( 'NONE',  ( 0.000000000000000000, 0.000000000000000000, 1.000000000000000000 ) ) ;
#23421=ORIENTED_EDGE ( 'NONE', *, *, #6081, .F. ) ;
#23425=EDGE_CURVE ( 'NONE', #38690, #2973, #4570, .T. ) ;
#23514=CARTESIAN_POINT ( 'NONE',  ( -10.50000000000000178, 1.285879139104721028E-15, -1.199999999999999956 ) ) ;
#23553=ORIENTED_EDGE ( 'NONE', *, *, #43021, .F. ) ;
#23582=AXIS2_PLACEMENT_3D ( 'NONE', #22112, #38631, #8757 ) ;
#23596=AXIS2_PLACEMENT_3D ( 'NONE', #14479, #37994, #898 ) ;
#23620=EDGE_LOOP ( 'NONE', ( #14915, #22858, #3318, #27077 ) ) ;
#23633=EDGE_CURVE ( 'NONE', #35327, #31991, #5975, .T. ) ;
#23667=EDGE_CURVE ( 'NONE', #31449, #11136, #7142, .T. ) ;
#23727=LINE ( 'NONE', #23514, #25678 ) ;
#23744=CARTESIAN_POINT ( 'NONE',  ( 0.000000000000000000, 0.000000000000000000, -1.199999999999999956 ) ) ;
#23766=DIRECTION ( 'NONE',  ( 0.1305261922200494362, 0.9914448613738107152, -0.000000000000000000 ) ) ;
#23780=DIRECTION ( 'NONE',  ( 1.000000000000000000, 0.000000000000000000, 0.000000000000000000 ) ) ;
#23832=ORIENTED_EDGE ( 'NONE', *, *, #17519, .T. ) ;
#23864=DIRECTION ( 'NONE',  ( 0.000000000000000000, 0.000000000000000000, 1.000000000000000000 ) ) ;
#23884=ORIENTED_EDGE ( 'NONE', *, *, #41226, .T. ) ;
#23894=SURFACE_STYLE_USAGE ( .BOTH. , #24552 ) ;
#23909=ADVANCED_FACE ( 'NONE', ( #14365 ), #28106, .T. ) ;
#23938=EDGE_CURVE ( 'NONE', #24620, #41098, #41602, .T. ) ;
#24092=ORIENTED_EDGE ( 'NONE', *, *, #37073, .T. ) ;
#24133=ADVANCED_FACE ( 'NONE', ( #2579 ), #35114, .F. ) ;
#24250=CARTESIAN_POINT ( 'NONE',  ( 0.5999999999999994227, -12.75000000000000000, -1.199999999999999956 ) ) ;
#24398=( NAMED_UNIT ( * ) SI_UNIT ( $, .STERADIAN. ) SOLID_ANGLE_UNIT ( ) );
#24531=ORIENTED_EDGE ( 'NONE', *, *, #5828, .T. ) ;
#24552=SURFACE_SIDE_STYLE ('',( #21074 ) ) ;
#24601=CIRCLE ( 'NONE', #32902, 1.000000000000000444 ) ;
#24620=VERTEX_POINT ( 'NONE', #6222 ) ;
#24715=LINE ( 'NONE', #1100, #20613 ) ;
#24740=CARTESIAN_POINT ( 'NONE',  ( -0.2142857142857142738, -10.49781318335647917, -1.199999999999999956 ) ) ;
#24744=DIRECTION ( 'NONE',  ( 0.000000000000000000, 0.000000000000000000, 1.000000000000000000 ) ) ;
#24792=EDGE_CURVE ( 'NONE', #18000, #30690, #2838, .T. ) ;
#24829=VECTOR ( 'NONE', #41818, 1000.000000000000000 ) ;
#24852=EDGE_CURVE ( 'NONE', #26713, #42086, #32966, .T. ) ;
#24932=AXIS2_PLACEMENT_3D ( 'NONE', #34987, #14733, #28040 ) ;
#24938=CARTESIAN_POINT ( 'NONE',  ( -1.600000000000000089, -12.75000000000000000, -1.199999999999999956 ) ) ;
#25000=ORIENTED_EDGE ( 'NONE', *, *, #23425, .F. ) ;
#25179=EDGE_CURVE ( 'NONE', #2427, #2530, #19869, .T. ) ;
#25220=CYLINDRICAL_SURFACE ( 'NONE', #36762, 1.000000000000000666 ) ;
#25319=DIRECTION ( 'NONE',  ( 0.000000000000000000, 0.000000000000000000, 1.000000000000000000 ) ) ;
#25428=CARTESIAN_POINT ( 'NONE',  ( 0.000000000000000000, 0.000000000000000000, 0.000000000000000000 ) ) ;
#25521=CARTESIAN_POINT ( 'NONE',  ( -0.2999999999999999889, -14.69693845669906906, -1.199999999999999956 ) ) ;
#25568=DIRECTION ( 'NONE',  ( 1.000000000000000000, 0.000000000000000000, 0.000000000000000000 ) ) ;
#25658=ORIENTED_EDGE ( 'NONE', *, *, #26290, .F. ) ;
#25678=VECTOR ( 'NONE', #20676, 1000.000000000000000 ) ;
#25693=CIRCLE ( 'NONE', #31928, 0.7500000000000006661 ) ;
#25734=EDGE_LOOP ( 'NONE', ( #5099, #38124, #7949, #29144 ) ) ;
#25850=DIRECTION ( 'NONE',  ( 0.000000000000000000, 0.000000000000000000, 1.000000000000000000 ) ) ;
#25923=ORIENTED_EDGE ( 'NONE', *, *, #27894, .T. ) ;
#25925=ADVANCED_FACE ( 'NONE', ( #20250 ), #30691, .T. ) ;
#25940=EDGE_LOOP ( 'NONE', ( #4811, #37699, #39127, #24092 ) ) ;
#26021=AXIS2_PLACEMENT_3D ( 'NONE', #14775, #34816, #4923 ) ;
#26041=LINE ( 'NONE', #2657, #32890 ) ;
#26049=FACE_BOUND ( 'NONE', #29635, .T. ) ;
#26063=( GEOMETRIC_REPRESENTATION_CONTEXT ( 3 ) GLOBAL_UNCERTAINTY_ASSIGNED_CONTEXT ( ( #13904 ) ) GLOBAL_UNIT_ASSIGNED_CONTEXT ( ( #34536, #27585, #14723 ) ) REPRESENTATION_CONTEXT ( 'NONE', 'WORKASPACE' ) );
#26147=EDGE_CURVE ( 'NONE', #38781, #3798, #11391, .T. ) ;
#26212=FACE_OUTER_BOUND ( 'NONE', #23005, .T. ) ;
#26222=CIRCLE ( 'NONE', #30400, 2.799122904894268071 ) ;
#26290=EDGE_CURVE ( 'NONE', #33425, #35058, #6203, .T. ) ;
#26318=ORIENTED_EDGE ( 'NONE', *, *, #43021, .T. ) ;
#26389=ORIENTED_EDGE ( 'NONE', *, *, #19708, .F. ) ;
#26542=CYLINDRICAL_SURFACE ( 'NONE', #4489, 0.7500000000000006661 ) ;
#26710=ORIENTED_EDGE ( 'NONE', *, *, #8076, .T. ) ;
#26713=VERTEX_POINT ( 'NONE', #32928 ) ;
#26726=CARTESIAN_POINT ( 'NONE',  ( 10.50000000000000178, 0.000000000000000000, -1.199999999999999956 ) ) ;
#26748=EDGE_CURVE ( 'NONE', #13428, #3211, #12842, .T. ) ;
#26999=PRODUCT_DEFINITION_SHAPE ( 'NONE', 'NONE',  #37893 ) ;
#27077=ORIENTED_EDGE ( 'NONE', *, *, #25179, .T. ) ;
#27101=CYLINDRICAL_SURFACE ( 'NONE', #3791, 10.50000000000000178 ) ;
#27121=DIRECTION ( 'NONE',  ( 1.000000000000000000, 0.000000000000000000, 0.000000000000000000 ) ) ;
#27141=VERTEX_POINT ( 'NONE', #12620 ) ;
#27142=CARTESIAN_POINT ( 'NONE',  ( 0.2142857142857142738, -10.49781318335647917, 0.000000000000000000 ) ) ;
#27149=VERTEX_POINT ( 'NONE', #25521 ) ;
#27290=DIRECTION ( 'NONE',  ( -0.000000000000000000, -0.000000000000000000, -1.000000000000000000 ) ) ;
#27490=CARTESIAN_POINT ( 'NONE',  ( 0.5999999999999994227, -12.75000000000000000, 0.000000000000000000 ) ) ;
#27502=MANIFOLD_SOLID_BREP ( 'Body', #28198 ) ;
#27514=EDGE_LOOP ( 'NONE', ( #14130, #18346, #41213, #29417 ) ) ;
#27534=ORIENTED_EDGE ( 'NONE', *, *, #28143, .F. ) ;
#27585=( NAMED_UNIT ( * ) PLANE_ANGLE_UNIT ( ) SI_UNIT ( $, .RADIAN. ) );
#27654=EDGE_LOOP ( 'NONE', ( #23421, #2112, #13515, #28883 ) ) ;
#27674=LINE ( 'NONE', #4739, #12647 ) ;
#27715=AXIS2_PLACEMENT_3D ( 'NONE', #33625, #17086, #34712 ) ;
#27818=CARTESIAN_POINT ( 'NONE',  ( -4.121423858225412573, -12.61643262889541184, -1.199999999999999956 ) ) ;
#27855=VECTOR ( 'NONE', #10095, 1000.000000000000114 ) ;
#27857=CARTESIAN_POINT ( 'NONE',  ( -0.2142857142857142738, -10.49781318335647917, -1.199999999999999956 ) ) ;
#27859=DIRECTION ( 'NONE',  ( 1.000000000000000000, 0.000000000000000000, 0.000000000000000000 ) ) ;
#27894=EDGE_CURVE ( 'NONE', #16799, #13177, #3564, .T. ) ;
#28003=ORIENTED_EDGE ( 'NONE', *, *, #4329, .F. ) ;
#28025=FILL_AREA_STYLE_COLOUR ( '', #7191 ) ;
#28040=DIRECTION ( 'NONE',  ( 1.000000000000000000, 0.000000000000000000, 0.000000000000000000 ) ) ;
#28083=SURFACE_STYLE_FILL_AREA ( #8417 ) ;
#28106=CYLINDRICAL_SURFACE ( 'NONE', #37372, 14.70000000000000107 ) ;
#28124=ORIENTED_EDGE ( 'NONE', *, *, #23667, .T. ) ;
#28143=EDGE_CURVE ( 'NONE', #27141, #15184, #3137, .T. ) ;
#28155=CYLINDRICAL_SURFACE ( 'NONE', #1529, 1.000000000000000444 ) ;
#28198=CLOSED_SHELL ( 'NONE', ( #9093, #21304, #7170, #6264, #35763, #2279, #36203, #35817, #25925, #17910, #6786, #24133, #16279, #843, #28866, #31956, #23909, #34898, #2843, #35453, #15260, #20811 ) ) ;
#28299=CARTESIAN_POINT ( 'NONE',  ( 0.000000000000000000, 0.000000000000000000, -1.199999999999999956 ) ) ;
#28496=VERTEX_POINT ( 'NONE', #1709 ) ;
#28512=EDGE_CURVE ( 'NONE', #3798, #38781, #7403, .T. ) ;
#28536=ORIENTED_EDGE ( 'NONE', *, *, #39383, .F. ) ;
#28604=DIRECTION ( 'NONE',  ( 1.000000000000000000, 0.000000000000000000, 0.000000000000000000 ) ) ;
#28619=DIRECTION ( 'NONE',  ( 0.000000000000000000, 0.000000000000000000, 1.000000000000000000 ) ) ;
#28635=LINE ( 'NONE', #42333, #8339 ) ;
#28797=EDGE_LOOP ( 'NONE', ( #4951, #29569, #29969, #42805 ) ) ;
#28866=ADVANCED_FACE ( 'NONE', ( #32205 ), #8865, .T. ) ;
#28883=ORIENTED_EDGE ( 'NONE', *, *, #39383, .T. ) ;
#28907=EDGE_LOOP ( 'NONE', ( #23553, #22015, #36964, #18352 ) ) ;
#28929=PLANE ( 'NONE',  #42893 ) ;
#28972=AXIS2_PLACEMENT_3D ( 'NONE', #37205, #30475, #4033 ) ;
#29029=LINE ( 'NONE', #17018, #6674 ) ;
#29040=DIRECTION ( 'NONE',  ( 0.000000000000000000, 0.000000000000000000, 1.000000000000000000 ) ) ;
#29124=CARTESIAN_POINT ( 'NONE',  ( 1.600000000000000089, -12.75000000000000000, 0.000000000000000000 ) ) ;
#29144=ORIENTED_EDGE ( 'NONE', *, *, #4134, .F. ) ;
#29149=CARTESIAN_POINT ( 'NONE',  ( 2.600000000000000533, -12.75000000000000000, 0.000000000000000000 ) ) ;
#29186=ORIENTED_EDGE ( 'NONE', *, *, #8214, .T. ) ;
#29197=EDGE_LOOP ( 'NONE', ( #40075, #34101, #36420, #42342 ) ) ;
#29322=AXIS2_PLACEMENT_3D ( 'NONE', #391, #35973, #6513 ) ;
#29412=PRODUCT ( 'circlip for shafts normal_din_Circlip DIN 471 - 22 x 1.2', 'circlip for shafts normal_din_Circlip DIN 471 - 22 x 1.2', '', ( #34920 ) ) ;
#29417=ORIENTED_EDGE ( 'NONE', *, *, #30910, .T. ) ;
#29518=DIRECTION ( 'NONE',  ( 1.000000000000000000, 0.000000000000000000, 0.000000000000000000 ) ) ;
#29569=ORIENTED_EDGE ( 'NONE', *, *, #10007, .F. ) ;
#29587=EDGE_CURVE ( 'NONE', #11136, #18380, #37346, .T. ) ;
#29635=EDGE_LOOP ( 'NONE', ( #7727, #42454 ) ) ;
#29689=VECTOR ( 'NONE', #39923, 1000.000000000000000 ) ;
#29692=AXIS2_PLACEMENT_3D ( 'NONE', #37995, #24744, #8119 ) ;
#29941=CARTESIAN_POINT ( 'NONE',  ( 3.413765605486547727, -14.29811891091961229, -1.199999999999999956 ) ) ;
#29969=ORIENTED_EDGE ( 'NONE', *, *, #18974, .T. ) ;
#29979=EDGE_CURVE ( 'NONE', #2427, #18000, #21521, .T. ) ;
#30001=ORIENTED_EDGE ( 'NONE', *, *, #41455, .T. ) ;
#30032=CYLINDRICAL_SURFACE ( 'NONE', #4845, 1.000000000000000444 ) ;
#30040=ORIENTED_EDGE ( 'NONE', *, *, #18295, .F. ) ;
#30072=DIRECTION ( 'NONE',  ( 0.000000000000000000, 0.000000000000000000, 1.000000000000000000 ) ) ;
#30099=DIRECTION ( 'NONE',  ( 0.1305261922200512403, -0.9914448613738104932, 0.000000000000000000 ) ) ;
#30108=CYLINDRICAL_SURFACE ( 'NONE', #19592, 12.55910585664918422 ) ;
#30136=ORIENTED_EDGE ( 'NONE', *, *, #3851, .F. ) ;
#30256=DIRECTION ( 'NONE',  ( 1.000000000000000000, 0.000000000000000000, 0.000000000000000000 ) ) ;
#30308=CARTESIAN_POINT ( 'NONE',  ( -6.896599878636567205, -12.98179148322719101, -1.199999999999999956 ) ) ;
#30400=AXIS2_PLACEMENT_3D ( 'NONE', #30308, #604, #1031 ) ;
#30475=DIRECTION ( 'NONE',  ( -0.000000000000000000, -0.000000000000000000, -1.000000000000000000 ) ) ;
#30535=CARTESIAN_POINT ( 'NONE',  ( 0.000000000000000000, 0.000000000000000000, 0.000000000000000000 ) ) ;
#30690=VERTEX_POINT ( 'NONE', #11464 ) ;
#30691=CYLINDRICAL_SURFACE ( 'NONE', #2956, 14.70000000000000107 ) ;
#30772=VECTOR ( 'NONE', #10106, 1000.000000000000114 ) ;
#30828=ORIENTED_EDGE ( 'NONE', *, *, #41735, .F. ) ;
#30869=ORIENTED_EDGE ( 'NONE', *, *, #10568, .T. ) ;
#30910=EDGE_CURVE ( 'NONE', #2973, #38690, #14215, .T. ) ;
#30978=STYLED_ITEM ( 'NONE', ( #38023 ), #20853 ) ;
#31143=ORIENTED_EDGE ( 'NONE', *, *, #32823, .F. ) ;
#31258=ORIENTED_EDGE ( 'NONE', *, *, #18974, .F. ) ;
#31262=FACE_OUTER_BOUND ( 'NONE', #25734, .T. ) ;
#31272=CIRCLE ( 'NONE', #7584, 0.7500000000000006661 ) ;
#31346=SURFACE_STYLE_USAGE ( .BOTH. , #11936 ) ;
#31358=CARTESIAN_POINT ( 'NONE',  ( -12.55910585664918422, 0.7408941433508191565, 0.000000000000000000 ) ) ;
#31384=EDGE_LOOP ( 'NONE', ( #10189, #15897, #25923, #2887 ) ) ;
#31443=DIRECTION ( 'NONE',  ( 1.000000000000000000, 0.000000000000000000, 0.000000000000000000 ) ) ;
#31449=VERTEX_POINT ( 'NONE', #3433 ) ;
#31572=VERTEX_POINT ( 'NONE', #39443 ) ;
#31579=CARTESIAN_POINT ( 'NONE',  ( 0.000000000000000000, 0.000000000000000000, -1.199999999999999956 ) ) ;
#31619=LINE ( 'NONE', #34676, #4910 ) ;
#31630=ORIENTED_EDGE ( 'NONE', *, *, #18295, .T. ) ;
#31653=SHAPE_DEFINITION_REPRESENTATION ( #26999, #16840 ) ;
#31751=DIRECTION ( 'NONE',  ( 0.000000000000000000, 0.000000000000000000, 1.000000000000000000 ) ) ;
#31805=CIRCLE ( 'NONE', #32503, 14.70000000000000107 ) ;
#31808=CARTESIAN_POINT ( 'NONE',  ( -10.50000000000000178, 1.285879139104721028E-15, -1.199999999999999956 ) ) ;
#31823=ORIENTED_EDGE ( 'NONE', *, *, #4329, .T. ) ;
#31928=AXIS2_PLACEMENT_3D ( 'NONE', #16785, #30072, #13494 ) ;
#31956=ADVANCED_FACE ( 'NONE', ( #16531 ), #26542, .T. ) ;
#31982=CARTESIAN_POINT ( 'NONE',  ( -4.121423858225412573, -12.61643262889541184, -1.199999999999999956 ) ) ;
#31991=VERTEX_POINT ( 'NONE', #39387 ) ;
#32134=EDGE_CURVE ( 'NONE', #35058, #28496, #4633, .T. ) ;
#32152=DIRECTION ( 'NONE',  ( 0.000000000000000000, 0.000000000000000000, 1.000000000000000000 ) ) ;
#32184=FACE_BOUND ( 'NONE', #5334, .T. ) ;
#32191=ORIENTED_EDGE ( 'NONE', *, *, #19700, .T. ) ;
#32205=FACE_OUTER_BOUND ( 'NONE', #1905, .T. ) ;
#32282=ORIENTED_EDGE ( 'NONE', *, *, #26748, .T. ) ;
#32307=DIRECTION ( 'NONE',  ( 1.000000000000000000, 0.000000000000000000, 0.000000000000000000 ) ) ;
#32503=AXIS2_PLACEMENT_3D ( 'NONE', #30535, #37052, #40525 ) ;
#32643=DIRECTION ( 'NONE',  ( 1.000000000000000000, 0.000000000000000000, 0.000000000000000000 ) ) ;
#32654=CARTESIAN_POINT ( 'NONE',  ( 4.121423858225410797, -12.61643262889541006, -1.199999999999999956 ) ) ;
#32823=EDGE_CURVE ( 'NONE', #3211, #35058, #19269, .T. ) ;
#32837=EDGE_CURVE ( 'NONE', #33425, #21541, #29029, .T. ) ;
#32890=VECTOR ( 'NONE', #6167, 1000.000000000000000 ) ;
#32902=AXIS2_PLACEMENT_3D ( 'NONE', #24938, #37963, #31443 ) ;
#32928=CARTESIAN_POINT ( 'NONE',  ( -0.5999999999999996447, -12.75000000000000000, -1.199999999999999956 ) ) ;
#32936=DIRECTION ( 'NONE',  ( 0.02040816326530612776, -0.9997917317482359900, 0.000000000000000000 ) ) ;
#32957=ORIENTED_EDGE ( 'NONE', *, *, #17519, .F. ) ;
#32966=LINE ( 'NONE', #3045, #3175 ) ;
#33145=CARTESIAN_POINT ( 'NONE',  ( 0.000000000000000000, 0.7408941433508176022, -1.199999999999999956 ) ) ;
#33171=ORIENTED_EDGE ( 'NONE', *, *, #26290, .T. ) ;
#33237=LINE ( 'NONE', #27142, #27855 ) ;
#33250=CARTESIAN_POINT ( 'NONE',  ( -3.413765605486552168, -14.29811891091961407, 0.000000000000000000 ) ) ;
#33299=DIRECTION ( 'NONE',  ( 0.000000000000000000, 0.000000000000000000, 1.000000000000000000 ) ) ;
#33345=DIRECTION ( 'NONE',  ( -0.000000000000000000, -0.000000000000000000, -1.000000000000000000 ) ) ;
#33412=ORIENTED_EDGE ( 'NONE', *, *, #33533, .F. ) ;
#33425=VERTEX_POINT ( 'NONE', #39616 ) ;
#33455=EDGE_CURVE ( 'NONE', #27141, #21142, #43109, .T. ) ;
#33479=EDGE_CURVE ( 'NONE', #4089, #16799, #5252, .T. ) ;
#33491=ORIENTED_EDGE ( 'NONE', *, *, #10678, .T. ) ;
#33533=EDGE_CURVE ( 'NONE', #11136, #14824, #9410, .T. ) ;
#33625=CARTESIAN_POINT ( 'NONE',  ( 0.000000000000000000, 0.7408941433508176022, -1.199999999999999956 ) ) ;
#33672=( NAMED_UNIT ( * ) SI_UNIT ( $, .STERADIAN. ) SOLID_ANGLE_UNIT ( ) );
#33687=VECTOR ( 'NONE', #18926, 1000.000000000000000 ) ;
#33709=LINE ( 'NONE', #14110, #13304 ) ;
#33776=EDGE_LOOP ( 'NONE', ( #15221, #18853, #43045, #7895 ) ) ;
#33788=STYLED_ITEM ( 'NONE', ( #21784 ), #27502 ) ;
#33823=EDGE_LOOP ( 'NONE', ( #11908, #28536, #23884, #13670 ) ) ;
#33964=DIRECTION ( 'NONE',  ( 1.000000000000000000, 0.000000000000000000, 0.000000000000000000 ) ) ;
#34101=ORIENTED_EDGE ( 'NONE', *, *, #25179, .F. ) ;
#34287=VECTOR ( 'NONE', #2790, 1000.000000000000000 ) ;
#34325=CARTESIAN_POINT ( 'NONE',  ( -5.639656061357299244, -10.48075544252182922, 0.000000000000000000 ) ) ;
#34393=FACE_OUTER_BOUND ( 'NONE', #23620, .T. ) ;
#34536=( LENGTH_UNIT ( ) NAMED_UNIT ( * ) SI_UNIT ( .MILLI., .METRE. ) );
#34616=PLANE ( 'NONE',  #41558 ) ;
#34619=ORIENTED_EDGE ( 'NONE', *, *, #6183, .F. ) ;
#34676=CARTESIAN_POINT ( 'NONE',  ( 3.983177536951266529, -13.66651769228263191, -1.199999999999999956 ) ) ;
#34682=FACE_OUTER_BOUND ( 'NONE', #4148, .T. ) ;
#34712=DIRECTION ( 'NONE',  ( 1.000000000000000000, 0.000000000000000000, 0.000000000000000000 ) ) ;
#34737=CYLINDRICAL_SURFACE ( 'NONE', #23596, 10.50000000000000178 ) ;
#34764=SHAPE_REPRESENTATION_RELATIONSHIP ( 'NONE' , 'NONE' ,  #16840, #20853 ) ;
#34769=PLANE ( 'NONE',  #7206 ) ;
#34816=DIRECTION ( 'NONE',  ( 0.000000000000000000, 0.000000000000000000, 1.000000000000000000 ) ) ;
#34817=DIRECTION ( 'NONE',  ( 1.000000000000000000, 0.000000000000000000, 0.000000000000000000 ) ) ;
#34898=ADVANCED_FACE ( 'NONE', ( #34393 ), #34616, .T. ) ;
#34920=PRODUCT_CONTEXT ( 'NONE', #41755, 'mechanical' ) ;
#34952=LINE ( 'NONE', #5063, #38962 ) ;
#34985=ORIENTED_EDGE ( 'NONE', *, *, #32134, .T. ) ;
#34987=CARTESIAN_POINT ( 'NONE',  ( 0.000000000000000000, 0.7408941433508176022, 0.000000000000000000 ) ) ;
#35058=VERTEX_POINT ( 'NONE', #19366 ) ;
#35105=DIRECTION ( 'NONE',  ( 0.000000000000000000, 0.000000000000000000, 1.000000000000000000 ) ) ;
#35114=CYLINDRICAL_SURFACE ( 'NONE', #10212, 2.799122904894268071 ) ;
#35259=ORIENTED_EDGE ( 'NONE', *, *, #32134, .F. ) ;
#35327=VERTEX_POINT ( 'NONE', #8176 ) ;
#35365=VECTOR ( 'NONE', #32936, 1000.000000000000114 ) ;
#35370=CIRCLE ( 'NONE', #17292, 10.50000000000000178 ) ;
#35386=DIRECTION ( 'NONE',  ( 0.000000000000000000, 0.000000000000000000, 1.000000000000000000 ) ) ;
#35453=ADVANCED_FACE ( 'NONE', ( #26049, #12744, #36057 ), #38908, .T. ) ;
#35541=CARTESIAN_POINT ( 'NONE',  ( -6.896599878636567205, -12.98179148322719101, 0.000000000000000000 ) ) ;
#35737=CARTESIAN_POINT ( 'NONE',  ( -6.896599878636567205, -12.98179148322719101, -1.199999999999999956 ) ) ;
#35763=ADVANCED_FACE ( 'NONE', ( #31262 ), #34737, .F. ) ;
#35814=DIRECTION ( 'NONE',  ( 0.000000000000000000, 0.000000000000000000, 1.000000000000000000 ) ) ;
#35817=ADVANCED_FACE ( 'NONE', ( #37778 ), #7897, .T. ) ;
#35870=CARTESIAN_POINT ( 'NONE',  ( 10.50000000000000178, 0.000000000000000000, -1.199999999999999956 ) ) ;
#35925=AXIS2_PLACEMENT_3D ( 'NONE', #40296, #33345, #37036 ) ;
#35973=DIRECTION ( 'NONE',  ( 0.000000000000000000, 0.000000000000000000, 1.000000000000000000 ) ) ;
#36057=FACE_OUTER_BOUND ( 'NONE', #2135, .T. ) ;
#36155=CARTESIAN_POINT ( 'NONE',  ( 10.50000000000000178, 0.000000000000000000, 0.000000000000000000 ) ) ;
#36203=ADVANCED_FACE ( 'NONE', ( #26212 ), #6336, .F. ) ;
#36274=ORIENTED_EDGE ( 'NONE', *, *, #23633, .T. ) ;
#36420=ORIENTED_EDGE ( 'NONE', *, *, #29979, .T. ) ;
#36443=EDGE_CURVE ( 'NONE', #28496, #41098, #31272, .T. ) ;
#36459=VERTEX_POINT ( 'NONE', #5012 ) ;
#36480=DIRECTION ( 'NONE',  ( 0.000000000000000000, 0.000000000000000000, 1.000000000000000000 ) ) ;
#36639=DIRECTION ( 'NONE',  ( 1.000000000000000000, 0.000000000000000000, 0.000000000000000000 ) ) ;
#36736=VECTOR ( 'NONE', #23864, 1000.000000000000000 ) ;
#36762=AXIS2_PLACEMENT_3D ( 'NONE', #11892, #32152, #12103 ) ;
#36866=DIRECTION ( 'NONE',  ( -0.000000000000000000, -0.000000000000000000, -1.000000000000000000 ) ) ;
#36956=AXIS2_PLACEMENT_3D ( 'NONE', #15527, #29040, #25568 ) ;
#36962=ORIENTED_EDGE ( 'NONE', *, *, #27894, .F. ) ;
#36964=ORIENTED_EDGE ( 'NONE', *, *, #24852, .T. ) ;
#36976=EDGE_CURVE ( 'NONE', #12248, #2530, #33237, .T. ) ;
#37015=DIRECTION ( 'NONE',  ( 0.000000000000000000, 0.000000000000000000, 1.000000000000000000 ) ) ;
#37026=EDGE_LOOP ( 'NONE', ( #9773, #2599 ) ) ;
#37036=DIRECTION ( 'NONE',  ( 1.000000000000000000, 0.000000000000000000, 0.000000000000000000 ) ) ;
#37052=DIRECTION ( 'NONE',  ( 0.000000000000000000, 0.000000000000000000, 1.000000000000000000 ) ) ;
#37056=ORIENTED_EDGE ( 'NONE', *, *, #36976, .T. ) ;
#37073=EDGE_CURVE ( 'NONE', #14824, #23300, #34952, .T. ) ;
#37205=CARTESIAN_POINT ( 'NONE',  ( 0.000000000000000000, 0.000000000000000000, -1.199999999999999956 ) ) ;
#37211=DIRECTION ( 'NONE',  ( 0.000000000000000000, 0.000000000000000000, 1.000000000000000000 ) ) ;
#37346=LINE ( 'NONE', #469, #36736 ) ;
#37372=AXIS2_PLACEMENT_3D ( 'NONE', #31579, #1890, #11961 ) ;
#37649=( NAMED_UNIT ( * ) PLANE_ANGLE_UNIT ( ) SI_UNIT ( $, .RADIAN. ) );
#37664=ORIENTED_EDGE ( 'NONE', *, *, #6196, .T. ) ;
#37699=ORIENTED_EDGE ( 'NONE', *, *, #29587, .F. ) ;
#37778=FACE_OUTER_BOUND ( 'NONE', #33823, .T. ) ;
#37781=ORIENTED_EDGE ( 'NONE', *, *, #6183, .T. ) ;
#37803=ORIENTED_EDGE ( 'NONE', *, *, #2891, .T. ) ;
#37854=FACE_OUTER_BOUND ( 'NONE', #10395, .T. ) ;
#37893=PRODUCT_DEFINITION ( 'UNKNOWN', '', #42068, #10393 ) ;
#37941=DIRECTION ( 'NONE',  ( 0.000000000000000000, 0.000000000000000000, 1.000000000000000000 ) ) ;
#37963=DIRECTION ( 'NONE',  ( 0.000000000000000000, 0.000000000000000000, 1.000000000000000000 ) ) ;
#37972=CARTESIAN_POINT ( 'NONE',  ( 2.600000000000000533, -12.75000000000000000, -1.199999999999999956 ) ) ;
#37977=VECTOR ( 'NONE', #40255, 1000.000000000000114 ) ;
#37994=DIRECTION ( 'NONE',  ( 0.000000000000000000, 0.000000000000000000, 1.000000000000000000 ) ) ;
#37995=CARTESIAN_POINT ( 'NONE',  ( 1.600000000000000089, -12.75000000000000000, 0.000000000000000000 ) ) ;
#38023=PRESENTATION_STYLE_ASSIGNMENT (( #23894 ) ) ;
#38124=ORIENTED_EDGE ( 'NONE', *, *, #1251, .T. ) ;
#38175=CIRCLE ( 'NONE', #6116, 10.50000000000000178 ) ;
#38380=CARTESIAN_POINT ( 'NONE',  ( 0.000000000000000000, 0.7408941433508176022, -1.199999999999999956 ) ) ;
#38631=DIRECTION ( 'NONE',  ( 0.000000000000000000, 0.000000000000000000, 1.000000000000000000 ) ) ;
#38690=VERTEX_POINT ( 'NONE', #27490 ) ;
#38743=CARTESIAN_POINT ( 'NONE',  ( 0.000000000000000000, 0.000000000000000000, 0.000000000000000000 ) ) ;
#38781=VERTEX_POINT ( 'NONE', #24250 ) ;
#38819=ORIENTED_EDGE ( 'NONE', *, *, #33455, .T. ) ;
#38908=PLANE ( 'NONE',  #12410 ) ;
#38955=DIRECTION ( 'NONE',  ( -0.000000000000000000, -0.000000000000000000, -1.000000000000000000 ) ) ;
#38962=VECTOR ( 'NONE', #11857, 1000.000000000000000 ) ;
#39127=ORIENTED_EDGE ( 'NONE', *, *, #33533, .T. ) ;
#39154=ORIENTED_EDGE ( 'NONE', *, *, #10007, .T. ) ;
#39236=AXIS2_PLACEMENT_3D ( 'NONE', #29124, #36480, #22591 ) ;
#39261=VERTEX_POINT ( 'NONE', #43095 ) ;
#39297=EDGE_LOOP ( 'NONE', ( #34619, #5310, #31630, #17239 ) ) ;
#39383=EDGE_CURVE ( 'NONE', #27149, #39261, #33709, .T. ) ;
#39387=CARTESIAN_POINT ( 'NONE',  ( -10.50000000000000178, 1.285879139104721028E-15, 0.000000000000000000 ) ) ;
#39443=CARTESIAN_POINT ( 'NONE',  ( -2.600000000000000533, -12.75000000000000000, -1.199999999999999956 ) ) ;
#39515=ORIENTED_EDGE ( 'NONE', *, *, #16197, .T. ) ;
#39616=CARTESIAN_POINT ( 'NONE',  ( -4.121423858225412573, -12.61643262889541184, -1.199999999999999956 ) ) ;
#39773=ORIENTED_EDGE ( 'NONE', *, *, #23667, .F. ) ;
#39923=DIRECTION ( 'NONE',  ( 0.000000000000000000, 0.000000000000000000, 1.000000000000000000 ) ) ;
#39976=CARTESIAN_POINT ( 'NONE',  ( -0.2142857142857142738, -10.49781318335647917, -1.199999999999999956 ) ) ;
#40049=VECTOR ( 'NONE', #20873, 1000.000000000000000 ) ;
#40075=ORIENTED_EDGE ( 'NONE', *, *, #4325, .F. ) ;
#40107=CIRCLE ( 'NONE', #1794, 14.70000000000000107 ) ;
#40109=DIRECTION ( 'NONE',  ( 1.000000000000000000, 0.000000000000000000, 0.000000000000000000 ) ) ;
#40128=CARTESIAN_POINT ( 'NONE',  ( 0.000000000000000000, 0.000000000000000000, 0.000000000000000000 ) ) ;
#40210=AXIS2_PLACEMENT_3D ( 'NONE', #12475, #41696, #15120 ) ;
#40255=DIRECTION ( 'NONE',  ( 0.1305261922200512403, -0.9914448613738104932, 0.000000000000000000 ) ) ;
#40268=AXIS2_PLACEMENT_3D ( 'NONE', #24740, #41478, #21691 ) ;
#40296=CARTESIAN_POINT ( 'NONE',  ( 0.000000000000000000, 0.000000000000000000, 0.000000000000000000 ) ) ;
#40393=DIRECTION ( 'NONE',  ( 0.000000000000000000, 0.000000000000000000, 1.000000000000000000 ) ) ;
#40510=CARTESIAN_POINT ( 'NONE',  ( 4.121423858225410797, -12.61643262889541006, -1.199999999999999956 ) ) ;
#40525=DIRECTION ( 'NONE',  ( 1.000000000000000000, 0.000000000000000000, 0.000000000000000000 ) ) ;
#40536=AXIS2_PLACEMENT_3D ( 'NONE', #14036, #20825, #27121 ) ;
#40711=MECHANICAL_DESIGN_GEOMETRIC_PRESENTATION_REPRESENTATION('',(#33788),#21970);
#40809=ORIENTED_EDGE ( 'NONE', *, *, #41226, .F. ) ;
#40861=DIRECTION ( 'NONE',  ( 0.1305261922200512681, -0.9914448613738104932, 0.000000000000000000 ) ) ;
#40903=UNCERTAINTY_MEASURE_WITH_UNIT (LENGTH_MEASURE( 1.000000000000000082E-05 ), #23045, 'distance_accuracy_value', 'NONE');
#40904=DIRECTION ( 'NONE',  ( -0.000000000000000000, -0.000000000000000000, -1.000000000000000000 ) ) ;
#41098=VERTEX_POINT ( 'NONE', #33250 ) ;
#41142=CARTESIAN_POINT ( 'NONE',  ( 4.121423858225410797, -12.61643262889541006, -1.199999999999999956 ) ) ;
#41213=ORIENTED_EDGE ( 'NONE', *, *, #11394, .T. ) ;
#41226=EDGE_CURVE ( 'NONE', #27149, #1451, #20197, .T. ) ;
#41244=CARTESIAN_POINT ( 'NONE',  ( 12.55910585664918422, 0.7408941433508176022, 0.000000000000000000 ) ) ;
#41344=( LENGTH_UNIT ( ) NAMED_UNIT ( * ) SI_UNIT ( .MILLI., .METRE. ) );
#41428=CYLINDRICAL_SURFACE ( 'NONE', #3292, 12.55910585664918422 ) ;
#41453=CARTESIAN_POINT ( 'NONE',  ( -2.600000000000000533, -12.75000000000000000, -1.199999999999999956 ) ) ;
#41455=EDGE_CURVE ( 'NONE', #15184, #16399, #5035, .T. ) ;
#41478=DIRECTION ( 'NONE',  ( 0.9997917317482359900, -0.02040816326530612776, 0.000000000000000000 ) ) ;
#41502=AXIS2_PLACEMENT_3D ( 'NONE', #2436, #35814, #40109 ) ;
#41558=AXIS2_PLACEMENT_3D ( 'NONE', #11086, #21146, #17872 ) ;
#41602=LINE ( 'NONE', #17880, #6691 ) ;
#41656=DIRECTION ( 'NONE',  ( 0.000000000000000000, 0.000000000000000000, 1.000000000000000000 ) ) ;
#41696=DIRECTION ( 'NONE',  ( 0.000000000000000000, 0.000000000000000000, 1.000000000000000000 ) ) ;
#41735=EDGE_CURVE ( 'NONE', #31572, #26713, #24601, .T. ) ;
#41755=APPLICATION_CONTEXT ( 'automotive_design' ) ;
#41818=DIRECTION ( 'NONE',  ( 0.000000000000000000, 0.000000000000000000, 1.000000000000000000 ) ) ;
#41869=ORIENTED_EDGE ( 'NONE', *, *, #8076, .F. ) ;
#41907=DIRECTION ( 'NONE',  ( 0.000000000000000000, 0.000000000000000000, 1.000000000000000000 ) ) ;
#41958=FACE_OUTER_BOUND ( 'NONE', #27514, .T. ) ;
#41962=DIRECTION ( 'NONE',  ( 1.000000000000000000, 0.000000000000000000, -0.000000000000000000 ) ) ;
#42068=PRODUCT_DEFINITION_FORMATION_WITH_SPECIFIED_SOURCE ( 'ANY', '', #29412, .NOT_KNOWN. ) ;
#42086=VERTEX_POINT ( 'NONE', #20745 ) ;
#42122=LINE ( 'NONE', #42551, #770 ) ;
#42333=CARTESIAN_POINT ( 'NONE',  ( -12.55910585664918422, 0.7408941433508191565, -1.199999999999999956 ) ) ;
#42342=ORIENTED_EDGE ( 'NONE', *, *, #24792, .T. ) ;
#42356=DIRECTION ( 'NONE',  ( 0.000000000000000000, 0.000000000000000000, 1.000000000000000000 ) ) ;
#42440=DIRECTION ( 'NONE',  ( 1.000000000000000000, 0.000000000000000000, 0.000000000000000000 ) ) ;
#42454=ORIENTED_EDGE ( 'NONE', *, *, #19700, .F. ) ;
#42464=ORIENTED_EDGE ( 'NONE', *, *, #37073, .F. ) ;
#42551=CARTESIAN_POINT ( 'NONE',  ( 0.5999999999999994227, -12.75000000000000000, -1.199999999999999956 ) ) ;
#42805=ORIENTED_EDGE ( 'NONE', *, *, #23938, .T. ) ;
#42893=AXIS2_PLACEMENT_3D ( 'NONE', #28299, #7978, #21341 ) ;
#42949=DIRECTION ( 'NONE',  ( 0.000000000000000000, 0.000000000000000000, 1.000000000000000000 ) ) ;
#43021=EDGE_CURVE ( 'NONE', #31572, #5899, #16488, .T. ) ;
#43045=ORIENTED_EDGE ( 'NONE', *, *, #2891, .F. ) ;
#43095=CARTESIAN_POINT ( 'NONE',  ( -0.2999999999999999889, -14.69693845669906906, 0.000000000000000000 ) ) ;
#43109=LINE ( 'NONE', #19392, #4624 ) ;
#43167=CARTESIAN_POINT ( 'NONE',  ( 3.239593890920906993, -13.56862304811759223, 0.000000000000000000 ) ) ;
ENDSEC;
END-ISO-10303-21;
